ISO-10303-21;
HEADER;
/* Generated by software containing ST-Developer
 * from STEP Tools, Inc. (www.steptools.com) 
 */

FILE_DESCRIPTION(
/* description */ ('Compact intermittent indexer'),
/* implementation_level */ '2;1');

FILE_NAME(
/* name */ 'Retaining collar (1).step',
/* time_stamp */ '2026-10-29T16:32:17-07:00',
/* author */ (''),
/* organization */ (''),
/* preprocessor_version */ 'ST-DEVELOPER v20.2',
/* originating_system */ 'Autodesk Translation Framework v15.17.0.0',
/* authorisation */ '');

FILE_SCHEMA (('AUTOMOTIVE_DESIGN { 1 0 10303 214 3 1 1 }'));
ENDSEC;

DATA;
#10=MECHANICAL_DESIGN_GEOMETRIC_PRESENTATION_REPRESENTATION('',(#287),#10837);
#231=SHAPE_REPRESENTATION_RELATIONSHIP('SRR','None',#10968,#255);
#255=ADVANCED_BREP_SHAPE_REPRESENTATION('',(#317),#10835);
#287=STYLED_ITEM('',(#11180),#317);
#317=MANIFOLD_SOLID_BREP('Body1',#5661);
#349=B_SPLINE_CURVE_WITH_KNOTS('',3,(#10540,#10541,#10542,#10543,#10544,
#10545,#10546,#10547,#10548,#10549,#10550,#10551,#10552,#10553,#10554,#10555,
#10556,#10557,#10558,#10559,#10560,#10561,#10562,#10563,#10564,#10565,#10566,
#10567,#10568,#10569,#10570,#10571,#10572,#10573),.UNSPECIFIED.,.T.,.F.,
(4,2,2,2,2,2,2,2,2,2,2,2,2,2,2,2,4),(0.,0.0623062782223143,0.124612556444629,
0.186916384615149,0.249220212785669,0.31152404095619,0.37382786912671,0.436134147349024,
0.498440425571339,0.560746703793653,0.623052982015967,0.685356810186488,
0.747660638357008,0.809964466527529,0.872268294698049,0.934574572920363,
0.996880851142678),.UNSPECIFIED.);
#350=B_SPLINE_CURVE_WITH_KNOTS('',3,(#10576,#10577,#10578,#10579,#10580,
#10581,#10582,#10583,#10584,#10585,#10586,#10587,#10588,#10589),
 .UNSPECIFIED.,.F.,.F.,(4,2,2,2,2,2,4),(0.618551524396292,0.626563103102765,
0.689203386094988,0.751843669087211,0.814483952079434,0.877124235071657,
0.88513581377813),.UNSPECIFIED.);
#351=B_SPLINE_CURVE_WITH_KNOTS('',3,(#10592,#10593,#10594,#10595,#10596,
#10597,#10598,#10599,#10600,#10601,#10602,#10603,#10604,#10605),
 .UNSPECIFIED.,.F.,.F.,(4,2,2,2,2,2,4),(0.117322411671484,0.125333990377958,
0.187974273370181,0.250614556362404,0.313254839354627,0.37589512234685,
0.383906701053322),.UNSPECIFIED.);
#352=B_SPLINE_CURVE_WITH_KNOTS('',3,(#10616,#10617,#10618,#10619,#10620,
#10621,#10622,#10623,#10624,#10625),.UNSPECIFIED.,.F.,.F.,(4,2,2,2,4),(0.,
0.0623062782223142,0.124612556444628,0.186916384615149,0.249220212785669),
 .UNSPECIFIED.);
#353=B_SPLINE_CURVE_WITH_KNOTS('',3,(#10627,#10628,#10629,#10630,#10631,
#10632,#10633,#10634,#10635,#10636),.UNSPECIFIED.,.F.,.F.,(4,2,2,2,4),(0.747660638357008,
0.809964466527528,0.872268294698049,0.934574572920363,0.996880851142677),
 .UNSPECIFIED.);
#354=B_SPLINE_CURVE_WITH_KNOTS('',3,(#10637,#10638,#10639,#10640,#10641,
#10642,#10643,#10644,#10645,#10646,#10647,#10648,#10649,#10650,#10651,#10652,
#10653,#10654),.UNSPECIFIED.,.F.,.F.,(4,2,2,2,2,2,2,2,4),(0.249220212785669,
0.31152404095619,0.37382786912671,0.436134147349024,0.498440425571339,0.560746703793653,
0.623052982015967,0.685356810186488,0.747660638357008),.UNSPECIFIED.);
#355=B_SPLINE_CURVE_WITH_KNOTS('',3,(#10658,#10659,#10660,#10661,#10662,
#10663,#10664,#10665),.UNSPECIFIED.,.F.,.F.,(4,2,2,4),(0.618551507245623,
0.626563103102765,0.689203386094988,0.751843669087211),.UNSPECIFIED.);
#356=B_SPLINE_CURVE_WITH_KNOTS('',3,(#10669,#10670,#10671,#10672,#10673,
#10674,#10675,#10676),.UNSPECIFIED.,.F.,.F.,(4,2,2,4),(0.250614556362404,
0.313254839354627,0.37589512234685,0.383906718203992),.UNSPECIFIED.);
#357=B_SPLINE_CURVE_WITH_KNOTS('',3,(#10677,#10678,#10679,#10680,#10681,
#10682,#10683,#10684),.UNSPECIFIED.,.F.,.F.,(4,2,2,4),(0.117322394520816,
0.125333990377958,0.187974273370181,0.250614556362404),.UNSPECIFIED.);
#358=B_SPLINE_CURVE_WITH_KNOTS('',3,(#10685,#10686,#10687,#10688,#10689,
#10690,#10691,#10692),.UNSPECIFIED.,.F.,.F.,(4,2,2,4),(0.751843669087211,
0.814483952079434,0.877124235071657,0.8851358309288),.UNSPECIFIED.);
#466=FACE_BOUND('',#1413,.T.);
#467=FACE_BOUND('',#1415,.T.);
#468=FACE_BOUND('',#1417,.T.);
#469=FACE_BOUND('',#1419,.T.);
#637=PLANE('',#6615);
#638=PLANE('',#6620);
#639=PLANE('',#6621);
#640=PLANE('',#6625);
#641=PLANE('',#6632);
#642=PLANE('',#6633);
#965=FACE_OUTER_BOUND('',#1406,.T.);
#966=FACE_OUTER_BOUND('',#1407,.T.);
#967=FACE_OUTER_BOUND('',#1408,.T.);
#968=FACE_OUTER_BOUND('',#1409,.T.);
#969=FACE_OUTER_BOUND('',#1410,.T.);
#970=FACE_OUTER_BOUND('',#1411,.T.);
#971=FACE_OUTER_BOUND('',#1412,.T.);
#972=FACE_OUTER_BOUND('',#1414,.T.);
#973=FACE_OUTER_BOUND('',#1416,.T.);
#974=FACE_OUTER_BOUND('',#1418,.T.);
#1406=EDGE_LOOP('',(#5068,#5069,#5070));
#1407=EDGE_LOOP('',(#5071,#5072,#5073,#5074,#5075,#5076,#5077,#5078));
#1408=EDGE_LOOP('',(#5079,#5080));
#1409=EDGE_LOOP('',(#5081,#5082));
#1410=EDGE_LOOP('',(#5083,#5084,#5085,#5086,#5087,#5088,#5089,#5090,#5091,
#5092,#5093));
#1411=EDGE_LOOP('',(#5094,#5095));
#1412=EDGE_LOOP('',(#5096,#5097,#5098,#5099,#5100,#5101,#5102,#5103,#5104,
#5105,#5106,#5107));
#1413=EDGE_LOOP('',(#5108,#5109,#5110,#5111));
#1414=EDGE_LOOP('',(#5112,#5113,#5114,#5115,#5116,#5117,#5118,#5119,#5120));
#1415=EDGE_LOOP('',(#5121));
#1416=EDGE_LOOP('',(#5122));
#1417=EDGE_LOOP('',(#5123));
#1418=EDGE_LOOP('',(#5124));
#1419=EDGE_LOOP('',(#5125));
#1760=LINE('',#10534,#2118);
#1761=LINE('',#10574,#2119);
#1762=LINE('',#10607,#2120);
#1763=LINE('',#10611,#2121);
#1764=LINE('',#10656,#2122);
#1765=LINE('',#10694,#2123);
#1766=LINE('',#10698,#2124);
#1767=LINE('',#10700,#2125);
#1768=LINE('',#10705,#2126);
#1769=LINE('',#10707,#2127);
#2118=VECTOR('',#8370,1.);
#2119=VECTOR('',#8377,0.165);
#2120=VECTOR('',#8382,1.);
#2121=VECTOR('',#8385,1.);
#2122=VECTOR('',#8390,0.165);
#2123=VECTOR('',#8395,1.);
#2124=VECTOR('',#8400,0.505);
#2125=VECTOR('',#8401,0.505);
#2126=VECTOR('',#8408,0.9);
#2127=VECTOR('',#8409,0.9);
#2470=CIRCLE('',#6616,0.165);
#2471=CIRCLE('',#6617,0.165);
#2472=CIRCLE('',#6619,0.165);
#2473=CIRCLE('',#6622,0.165);
#2474=CIRCLE('',#6624,0.165);
#2475=CIRCLE('',#6627,0.505);
#2476=CIRCLE('',#6628,0.505);
#2477=CIRCLE('',#6630,0.9);
#2478=CIRCLE('',#6631,0.9);
#2942=VERTEX_POINT('',#10532);
#2943=VERTEX_POINT('',#10533);
#2944=VERTEX_POINT('',#10535);
#2945=VERTEX_POINT('',#10539);
#2946=VERTEX_POINT('',#10575);
#2947=VERTEX_POINT('',#10590);
#2948=VERTEX_POINT('',#10609);
#2949=VERTEX_POINT('',#10610);
#2950=VERTEX_POINT('',#10614);
#2951=VERTEX_POINT('',#10615);
#2952=VERTEX_POINT('',#10626);
#2953=VERTEX_POINT('',#10655);
#2954=VERTEX_POINT('',#10657);
#2955=VERTEX_POINT('',#10666);
#2956=VERTEX_POINT('',#10668);
#2957=VERTEX_POINT('',#10696);
#2958=VERTEX_POINT('',#10699);
#2959=VERTEX_POINT('',#10703);
#2960=VERTEX_POINT('',#10706);
#3656=EDGE_CURVE('',#2942,#2943,#1760,.T.);
#3657=EDGE_CURVE('',#2944,#2942,#2470,.T.);
#3658=EDGE_CURVE('',#2943,#2944,#2471,.T.);
#3659=EDGE_CURVE('',#2945,#2945,#349,.T.);
#3660=EDGE_CURVE('',#2945,#2944,#1761,.T.);
#3661=EDGE_CURVE('',#2946,#2942,#350,.T.);
#3662=EDGE_CURVE('',#2946,#2947,#2472,.T.);
#3663=EDGE_CURVE('',#2943,#2947,#351,.T.);
#3664=EDGE_CURVE('',#2947,#2946,#1762,.T.);
#3665=EDGE_CURVE('',#2948,#2949,#1763,.T.);
#3666=EDGE_CURVE('',#2949,#2948,#2473,.T.);
#3667=EDGE_CURVE('',#2950,#2951,#352,.T.);
#3668=EDGE_CURVE('',#2952,#2950,#353,.T.);
#3669=EDGE_CURVE('',#2951,#2952,#354,.T.);
#3670=EDGE_CURVE('',#2951,#2953,#1764,.T.);
#3671=EDGE_CURVE('',#2954,#2953,#355,.T.);
#3672=EDGE_CURVE('',#2954,#2955,#2474,.T.);
#3673=EDGE_CURVE('',#2956,#2955,#356,.T.);
#3674=EDGE_CURVE('',#2949,#2956,#357,.T.);
#3675=EDGE_CURVE('',#2953,#2948,#358,.T.);
#3676=EDGE_CURVE('',#2955,#2954,#1765,.T.);
#3677=EDGE_CURVE('',#2957,#2957,#2475,.T.);
#3678=EDGE_CURVE('',#2957,#2953,#1766,.T.);
#3679=EDGE_CURVE('',#2956,#2958,#1767,.T.);
#3680=EDGE_CURVE('',#2958,#2958,#2476,.T.);
#3681=EDGE_CURVE('',#2959,#2959,#2477,.T.);
#3682=EDGE_CURVE('',#2959,#2951,#1768,.T.);
#3683=EDGE_CURVE('',#2952,#2960,#1769,.T.);
#3684=EDGE_CURVE('',#2960,#2960,#2478,.T.);
#5068=ORIENTED_EDGE('',*,*,#3656,.F.);
#5069=ORIENTED_EDGE('',*,*,#3657,.F.);
#5070=ORIENTED_EDGE('',*,*,#3658,.F.);
#5071=ORIENTED_EDGE('',*,*,#3659,.F.);
#5072=ORIENTED_EDGE('',*,*,#3660,.T.);
#5073=ORIENTED_EDGE('',*,*,#3657,.T.);
#5074=ORIENTED_EDGE('',*,*,#3661,.F.);
#5075=ORIENTED_EDGE('',*,*,#3662,.T.);
#5076=ORIENTED_EDGE('',*,*,#3663,.F.);
#5077=ORIENTED_EDGE('',*,*,#3658,.T.);
#5078=ORIENTED_EDGE('',*,*,#3660,.F.);
#5079=ORIENTED_EDGE('',*,*,#3664,.F.);
#5080=ORIENTED_EDGE('',*,*,#3662,.F.);
#5081=ORIENTED_EDGE('',*,*,#3665,.F.);
#5082=ORIENTED_EDGE('',*,*,#3666,.F.);
#5083=ORIENTED_EDGE('',*,*,#3667,.F.);
#5084=ORIENTED_EDGE('',*,*,#3668,.F.);
#5085=ORIENTED_EDGE('',*,*,#3669,.F.);
#5086=ORIENTED_EDGE('',*,*,#3670,.T.);
#5087=ORIENTED_EDGE('',*,*,#3671,.F.);
#5088=ORIENTED_EDGE('',*,*,#3672,.T.);
#5089=ORIENTED_EDGE('',*,*,#3673,.F.);
#5090=ORIENTED_EDGE('',*,*,#3674,.F.);
#5091=ORIENTED_EDGE('',*,*,#3666,.T.);
#5092=ORIENTED_EDGE('',*,*,#3675,.F.);
#5093=ORIENTED_EDGE('',*,*,#3670,.F.);
#5094=ORIENTED_EDGE('',*,*,#3676,.F.);
#5095=ORIENTED_EDGE('',*,*,#3672,.F.);
#5096=ORIENTED_EDGE('',*,*,#3677,.F.);
#5097=ORIENTED_EDGE('',*,*,#3678,.T.);
#5098=ORIENTED_EDGE('',*,*,#3675,.T.);
#5099=ORIENTED_EDGE('',*,*,#3665,.T.);
#5100=ORIENTED_EDGE('',*,*,#3674,.T.);
#5101=ORIENTED_EDGE('',*,*,#3679,.T.);
#5102=ORIENTED_EDGE('',*,*,#3680,.T.);
#5103=ORIENTED_EDGE('',*,*,#3679,.F.);
#5104=ORIENTED_EDGE('',*,*,#3673,.T.);
#5105=ORIENTED_EDGE('',*,*,#3676,.T.);
#5106=ORIENTED_EDGE('',*,*,#3671,.T.);
#5107=ORIENTED_EDGE('',*,*,#3678,.F.);
#5108=ORIENTED_EDGE('',*,*,#3663,.T.);
#5109=ORIENTED_EDGE('',*,*,#3664,.T.);
#5110=ORIENTED_EDGE('',*,*,#3661,.T.);
#5111=ORIENTED_EDGE('',*,*,#3656,.T.);
#5112=ORIENTED_EDGE('',*,*,#3681,.F.);
#5113=ORIENTED_EDGE('',*,*,#3682,.T.);
#5114=ORIENTED_EDGE('',*,*,#3669,.T.);
#5115=ORIENTED_EDGE('',*,*,#3683,.T.);
#5116=ORIENTED_EDGE('',*,*,#3684,.T.);
#5117=ORIENTED_EDGE('',*,*,#3683,.F.);
#5118=ORIENTED_EDGE('',*,*,#3668,.T.);
#5119=ORIENTED_EDGE('',*,*,#3667,.T.);
#5120=ORIENTED_EDGE('',*,*,#3682,.F.);
#5121=ORIENTED_EDGE('',*,*,#3659,.T.);
#5122=ORIENTED_EDGE('',*,*,#3681,.T.);
#5123=ORIENTED_EDGE('',*,*,#3677,.T.);
#5124=ORIENTED_EDGE('',*,*,#3684,.F.);
#5125=ORIENTED_EDGE('',*,*,#3680,.F.);
#5290=CYLINDRICAL_SURFACE('',#6618,0.165);
#5291=CYLINDRICAL_SURFACE('',#6623,0.165);
#5292=CYLINDRICAL_SURFACE('',#6626,0.505);
#5293=CYLINDRICAL_SURFACE('',#6629,0.9);
#5608=ADVANCED_FACE('',(#965),#637,.F.);
#5609=ADVANCED_FACE('',(#966),#5290,.F.);
#5610=ADVANCED_FACE('',(#967),#638,.F.);
#5611=ADVANCED_FACE('',(#968),#639,.F.);
#5612=ADVANCED_FACE('',(#969),#5291,.F.);
#5613=ADVANCED_FACE('',(#970),#640,.F.);
#5614=ADVANCED_FACE('',(#971,#466),#5292,.F.);
#5615=ADVANCED_FACE('',(#972,#467),#5293,.T.);
#5616=ADVANCED_FACE('',(#973,#468),#641,.T.);
#5617=ADVANCED_FACE('',(#974,#469),#642,.F.);
#5661=CLOSED_SHELL('',(#5608,#5609,#5610,#5611,#5612,#5613,#5614,#5615,
#5616,#5617));
#6614=AXIS2_PLACEMENT_3D('',#10530,#8366,#8367);
#6615=AXIS2_PLACEMENT_3D('',#10531,#8368,#8369);
#6616=AXIS2_PLACEMENT_3D('',#10536,#8371,#8372);
#6617=AXIS2_PLACEMENT_3D('',#10537,#8373,#8374);
#6618=AXIS2_PLACEMENT_3D('',#10538,#8375,#8376);
#6619=AXIS2_PLACEMENT_3D('',#10591,#8378,#8379);
#6620=AXIS2_PLACEMENT_3D('',#10606,#8380,#8381);
#6621=AXIS2_PLACEMENT_3D('',#10608,#8383,#8384);
#6622=AXIS2_PLACEMENT_3D('',#10612,#8386,#8387);
#6623=AXIS2_PLACEMENT_3D('',#10613,#8388,#8389);
#6624=AXIS2_PLACEMENT_3D('',#10667,#8391,#8392);
#6625=AXIS2_PLACEMENT_3D('',#10693,#8393,#8394);
#6626=AXIS2_PLACEMENT_3D('',#10695,#8396,#8397);
#6627=AXIS2_PLACEMENT_3D('',#10697,#8398,#8399);
#6628=AXIS2_PLACEMENT_3D('',#10701,#8402,#8403);
#6629=AXIS2_PLACEMENT_3D('',#10702,#8404,#8405);
#6630=AXIS2_PLACEMENT_3D('',#10704,#8406,#8407);
#6631=AXIS2_PLACEMENT_3D('',#10708,#8410,#8411);
#6632=AXIS2_PLACEMENT_3D('',#10709,#8412,#8413);
#6633=AXIS2_PLACEMENT_3D('',#10710,#8414,#8415);
#8366=DIRECTION('axis',(0.,0.,1.));
#8367=DIRECTION('refdir',(1.,0.,0.));
#8368=DIRECTION('center_axis',(0.,1.,0.));
#8369=DIRECTION('ref_axis',(1.,0.,0.));
#8370=DIRECTION('',(0.,0.,-1.));
#8371=DIRECTION('center_axis',(0.,1.,0.));
#8372=DIRECTION('ref_axis',(1.,0.,0.));
#8373=DIRECTION('center_axis',(0.,1.,0.));
#8374=DIRECTION('ref_axis',(1.,0.,0.));
#8375=DIRECTION('center_axis',(0.,1.,0.));
#8376=DIRECTION('ref_axis',(1.,0.,0.));
#8377=DIRECTION('',(0.,1.,0.));
#8378=DIRECTION('center_axis',(0.,1.,0.));
#8379=DIRECTION('ref_axis',(1.,0.,0.));
#8380=DIRECTION('center_axis',(0.,1.,0.));
#8381=DIRECTION('ref_axis',(1.,0.,0.));
#8382=DIRECTION('',(0.,0.,1.));
#8383=DIRECTION('center_axis',(1.,0.,0.));
#8384=DIRECTION('ref_axis',(0.,0.,-1.));
#8385=DIRECTION('',(0.,0.,-1.));
#8386=DIRECTION('center_axis',(1.,0.,0.));
#8387=DIRECTION('ref_axis',(0.,0.,-1.));
#8388=DIRECTION('center_axis',(1.,0.,0.));
#8389=DIRECTION('ref_axis',(0.,0.,-1.));
#8390=DIRECTION('',(1.,0.,0.));
#8391=DIRECTION('center_axis',(1.,0.,0.));
#8392=DIRECTION('ref_axis',(0.,0.,-1.));
#8393=DIRECTION('center_axis',(1.,0.,0.));
#8394=DIRECTION('ref_axis',(0.,0.,-1.));
#8395=DIRECTION('',(0.,0.,1.));
#8396=DIRECTION('center_axis',(0.,0.,1.));
#8397=DIRECTION('ref_axis',(1.,0.,0.));
#8398=DIRECTION('center_axis',(0.,0.,-1.));
#8399=DIRECTION('ref_axis',(1.,0.,0.));
#8400=DIRECTION('',(0.,0.,-1.));
#8401=DIRECTION('',(0.,0.,-1.));
#8402=DIRECTION('center_axis',(0.,0.,-1.));
#8403=DIRECTION('ref_axis',(1.,0.,0.));
#8404=DIRECTION('center_axis',(0.,0.,1.));
#8405=DIRECTION('ref_axis',(1.,0.,0.));
#8406=DIRECTION('center_axis',(0.,0.,1.));
#8407=DIRECTION('ref_axis',(1.,0.,0.));
#8408=DIRECTION('',(0.,0.,-1.));
#8409=DIRECTION('',(0.,0.,-1.));
#8410=DIRECTION('center_axis',(0.,0.,1.));
#8411=DIRECTION('ref_axis',(1.,0.,0.));
#8412=DIRECTION('center_axis',(0.,0.,1.));
#8413=DIRECTION('ref_axis',(1.,0.,0.));
#8414=DIRECTION('center_axis',(0.,0.,1.));
#8415=DIRECTION('ref_axis',(1.,0.,0.));
#10530=CARTESIAN_POINT('',(0.,0.,0.));
#10531=CARTESIAN_POINT('Origin',(4.24264068711929,-0.49,1.4));
#10532=CARTESIAN_POINT('',(4.12047276989058,-0.49,1.51090536506409));
#10533=CARTESIAN_POINT('',(4.12047276989058,-0.49,1.28909463493591));
#10534=CARTESIAN_POINT('',(4.12047276989058,-0.49,1.));
#10535=CARTESIAN_POINT('',(4.07764068711929,-0.49,1.4));
#10536=CARTESIAN_POINT('Origin',(4.24264068711929,-0.49,1.4));
#10537=CARTESIAN_POINT('Origin',(4.24264068711929,-0.49,1.4));
#10538=CARTESIAN_POINT('Origin',(4.24264068711929,-1.,1.4));
#10539=CARTESIAN_POINT('',(4.07764068711929,-0.884745726183518,1.4));
#10540=CARTESIAN_POINT('Ctrl Pts',(4.07764068711929,-0.884745726183518,
1.4));
#10541=CARTESIAN_POINT('Ctrl Pts',(4.07764068711929,-0.884745726183518,
1.42076875940744));
#10542=CARTESIAN_POINT('Ctrl Pts',(4.0818009681117,-0.885552759505265,1.44288889507334));
#10543=CARTESIAN_POINT('Ctrl Pts',(4.0986542169026,-0.888448648150043,1.48352706263377));
#10544=CARTESIAN_POINT('Ctrl Pts',(4.1113446933051,-0.890493604851638,1.50204924397737));
#10545=CARTESIAN_POINT('Ctrl Pts',(4.14059086811116,-0.894317234323941,
1.53129541878344));
#10546=CARTESIAN_POINT('Ctrl Pts',(4.1591132950286,-0.896347088899543,1.54398634598358));
#10547=CARTESIAN_POINT('Ctrl Pts',(4.19975231102587,-0.899208271860583,
1.56083992183864));
#10548=CARTESIAN_POINT('Ctrl Pts',(4.22187274439578,-0.9,1.565));
#10549=CARTESIAN_POINT('Ctrl Pts',(4.26340862984279,-0.9,1.565));
#10550=CARTESIAN_POINT('Ctrl Pts',(4.2855290632127,-0.899208271860583,1.56083992183864));
#10551=CARTESIAN_POINT('Ctrl Pts',(4.32616807920997,-0.896347088899543,
1.54398634598358));
#10552=CARTESIAN_POINT('Ctrl Pts',(4.34469050612741,-0.894317234323941,
1.53129541878344));
#10553=CARTESIAN_POINT('Ctrl Pts',(4.37393668093347,-0.890493604851638,
1.50204924397737));
#10554=CARTESIAN_POINT('Ctrl Pts',(4.38662715733598,-0.888448648150043,
1.48352706263377));
#10555=CARTESIAN_POINT('Ctrl Pts',(4.40348040612687,-0.885552759505265,
1.44288889507334));
#10556=CARTESIAN_POINT('Ctrl Pts',(4.40764068711929,-0.884745726183518,
1.42076875940744));
#10557=CARTESIAN_POINT('Ctrl Pts',(4.40764068711929,-0.884745726183518,
1.37923124059256));
#10558=CARTESIAN_POINT('Ctrl Pts',(4.40348040612687,-0.885552759505265,
1.35711110492666));
#10559=CARTESIAN_POINT('Ctrl Pts',(4.38662715733598,-0.888448648150043,
1.31647293736623));
#10560=CARTESIAN_POINT('Ctrl Pts',(4.37393668093347,-0.890493604851638,
1.29795075602263));
#10561=CARTESIAN_POINT('Ctrl Pts',(4.34469050612741,-0.894317234323941,
1.26870458121656));
#10562=CARTESIAN_POINT('Ctrl Pts',(4.32616807920997,-0.896347088899543,
1.25601365401642));
#10563=CARTESIAN_POINT('Ctrl Pts',(4.2855290632127,-0.899208271860583,1.23916007816136));
#10564=CARTESIAN_POINT('Ctrl Pts',(4.26340862984279,-0.9,1.235));
#10565=CARTESIAN_POINT('Ctrl Pts',(4.22187274439578,-0.9,1.235));
#10566=CARTESIAN_POINT('Ctrl Pts',(4.19975231102587,-0.899208271860583,
1.23916007816136));
#10567=CARTESIAN_POINT('Ctrl Pts',(4.1591132950286,-0.896347088899543,1.25601365401642));
#10568=CARTESIAN_POINT('Ctrl Pts',(4.14059086811116,-0.894317234323941,
1.26870458121656));
#10569=CARTESIAN_POINT('Ctrl Pts',(4.1113446933051,-0.890493604851638,1.29795075602263));
#10570=CARTESIAN_POINT('Ctrl Pts',(4.0986542169026,-0.888448648150043,1.31647293736623));
#10571=CARTESIAN_POINT('Ctrl Pts',(4.0818009681117,-0.885552759505265,1.35711110492666));
#10572=CARTESIAN_POINT('Ctrl Pts',(4.07764068711929,-0.884745726183518,
1.37923124059256));
#10573=CARTESIAN_POINT('Ctrl Pts',(4.07764068711929,-0.884745726183518,
1.4));
#10574=CARTESIAN_POINT('',(4.07764068711929,-1.,1.4));
#10575=CARTESIAN_POINT('',(4.36480860434799,-0.49,1.51090536506409));
#10576=CARTESIAN_POINT('Ctrl Pts',(4.36480860434799,-0.49,1.51090536506409));
#10577=CARTESIAN_POINT('Ctrl Pts',(4.36300960074558,-0.490448531679987,
1.51288705930464));
#10578=CARTESIAN_POINT('Ctrl Pts',(4.36117558368452,-0.490895245371684,
1.51481034122633));
#10579=CARTESIAN_POINT('Ctrl Pts',(4.34475268013864,-0.494795015531646,
1.5312332447722));
#10580=CARTESIAN_POINT('Ctrl Pts',(4.32630040214172,-0.498442514607594,
1.54390845611142));
#10581=CARTESIAN_POINT('Ctrl Pts',(4.28569028316644,-0.50357781976106,1.56079590960766));
#10582=CARTESIAN_POINT('Ctrl Pts',(4.26352078145003,-0.505,1.565));
#10583=CARTESIAN_POINT('Ctrl Pts',(4.22176059278855,-0.505,1.565));
#10584=CARTESIAN_POINT('Ctrl Pts',(4.19959109107213,-0.50357781976106,1.56079590960766));
#10585=CARTESIAN_POINT('Ctrl Pts',(4.15898097209685,-0.498442514607594,
1.54390845611142));
#10586=CARTESIAN_POINT('Ctrl Pts',(4.14052869409993,-0.494795015531646,
1.5312332447722));
#10587=CARTESIAN_POINT('Ctrl Pts',(4.12410579055406,-0.490895245371684,
1.51481034122633));
#10588=CARTESIAN_POINT('Ctrl Pts',(4.12227177349299,-0.490448531679987,
1.51288705930464));
#10589=CARTESIAN_POINT('Ctrl Pts',(4.12047276989058,-0.49,1.51090536506409));
#10590=CARTESIAN_POINT('',(4.36480860434799,-0.49,1.28909463493591));
#10591=CARTESIAN_POINT('Origin',(4.24264068711929,-0.49,1.4));
#10592=CARTESIAN_POINT('Ctrl Pts',(4.12047276989058,-0.49,1.28909463493591));
#10593=CARTESIAN_POINT('Ctrl Pts',(4.12227177349299,-0.490448531679987,
1.28711294069536));
#10594=CARTESIAN_POINT('Ctrl Pts',(4.12410579055406,-0.490895245371684,
1.28518965877367));
#10595=CARTESIAN_POINT('Ctrl Pts',(4.14052869409993,-0.494795015531646,
1.2687667552278));
#10596=CARTESIAN_POINT('Ctrl Pts',(4.15898097209685,-0.498442514607594,
1.25609154388858));
#10597=CARTESIAN_POINT('Ctrl Pts',(4.19959109107213,-0.50357781976106,1.23920409039234));
#10598=CARTESIAN_POINT('Ctrl Pts',(4.22176059278855,-0.505,1.235));
#10599=CARTESIAN_POINT('Ctrl Pts',(4.26352078145003,-0.505,1.235));
#10600=CARTESIAN_POINT('Ctrl Pts',(4.28569028316644,-0.50357781976106,1.23920409039234));
#10601=CARTESIAN_POINT('Ctrl Pts',(4.32630040214172,-0.498442514607594,
1.25609154388858));
#10602=CARTESIAN_POINT('Ctrl Pts',(4.34475268013864,-0.494795015531646,
1.2687667552278));
#10603=CARTESIAN_POINT('Ctrl Pts',(4.36117558368452,-0.490895245371684,
1.28518965877367));
#10604=CARTESIAN_POINT('Ctrl Pts',(4.36300960074558,-0.490448531679987,
1.28711294069536));
#10605=CARTESIAN_POINT('Ctrl Pts',(4.36480860434799,-0.49,1.28909463493591));
#10606=CARTESIAN_POINT('Origin',(4.24264068711929,-0.49,1.4));
#10607=CARTESIAN_POINT('',(4.36480860434799,-0.49,1.));
#10608=CARTESIAN_POINT('Origin',(3.75264069,0.,1.4));
#10609=CARTESIAN_POINT('',(3.75264069,0.122167928782887,1.51090535233657));
#10610=CARTESIAN_POINT('',(3.75264069,0.122167928782887,1.28909464766343));
#10611=CARTESIAN_POINT('',(3.75264069,0.122167928782887,1.));
#10612=CARTESIAN_POINT('Origin',(3.75264069,0.,1.4));
#10613=CARTESIAN_POINT('Origin',(3.24264069,0.,1.4));
#10614=CARTESIAN_POINT('',(3.35789496093577,0.165,1.4));
#10615=CARTESIAN_POINT('',(3.34264068711929,-2.02066721859313E-17,1.565));
#10616=CARTESIAN_POINT('Ctrl Pts',(3.35789496093577,0.165,1.4));
#10617=CARTESIAN_POINT('Ctrl Pts',(3.35789496093577,0.165,1.42076875940744));
#10618=CARTESIAN_POINT('Ctrl Pts',(3.35708792761402,0.160839719007584,1.44288889507334));
#10619=CARTESIAN_POINT('Ctrl Pts',(3.35419203896924,0.143986470216691,1.48352706263377));
#10620=CARTESIAN_POINT('Ctrl Pts',(3.35214708226765,0.131295993814186,1.50204924397737));
#10621=CARTESIAN_POINT('Ctrl Pts',(3.34832345279534,0.102049819008125,1.53129541878344));
#10622=CARTESIAN_POINT('Ctrl Pts',(3.34629359821974,0.0835273920906824,
1.54398634598358));
#10623=CARTESIAN_POINT('Ctrl Pts',(3.3434324152587,0.0428883760934127,1.56083992183864));
#10624=CARTESIAN_POINT('Ctrl Pts',(3.34264068711929,0.0207679427235068,
1.565));
#10625=CARTESIAN_POINT('Ctrl Pts',(3.34264068711929,2.77555756156289E-17,
1.565));
#10626=CARTESIAN_POINT('',(3.34264068711929,-7.59257876733526E-17,1.235));
#10627=CARTESIAN_POINT('Ctrl Pts',(3.34264068711929,-4.16333634234434E-17,
1.235));
#10628=CARTESIAN_POINT('Ctrl Pts',(3.34264068711929,0.0207679427235068,
1.235));
#10629=CARTESIAN_POINT('Ctrl Pts',(3.3434324152587,0.0428883760934127,1.23916007816136));
#10630=CARTESIAN_POINT('Ctrl Pts',(3.34629359821974,0.0835273920906823,
1.25601365401642));
#10631=CARTESIAN_POINT('Ctrl Pts',(3.34832345279534,0.102049819008125,1.26870458121656));
#10632=CARTESIAN_POINT('Ctrl Pts',(3.35214708226765,0.131295993814186,1.29795075602263));
#10633=CARTESIAN_POINT('Ctrl Pts',(3.35419203896924,0.143986470216691,1.31647293736623));
#10634=CARTESIAN_POINT('Ctrl Pts',(3.35708792761402,0.160839719007584,1.35711110492666));
#10635=CARTESIAN_POINT('Ctrl Pts',(3.35789496093577,0.165,1.37923124059256));
#10636=CARTESIAN_POINT('Ctrl Pts',(3.35789496093577,0.165,1.4));
#10637=CARTESIAN_POINT('Ctrl Pts',(3.34264068711929,2.77555756156289E-17,
1.565));
#10638=CARTESIAN_POINT('Ctrl Pts',(3.34264068711929,-0.0207679427235068,
1.565));
#10639=CARTESIAN_POINT('Ctrl Pts',(3.3434324152587,-0.0428883760934127,
1.56083992183864));
#10640=CARTESIAN_POINT('Ctrl Pts',(3.34629359821974,-0.0835273920906823,
1.54398634598358));
#10641=CARTESIAN_POINT('Ctrl Pts',(3.34832345279534,-0.102049819008125,
1.53129541878344));
#10642=CARTESIAN_POINT('Ctrl Pts',(3.35214708226765,-0.131295993814186,
1.50204924397737));
#10643=CARTESIAN_POINT('Ctrl Pts',(3.35419203896924,-0.143986470216691,
1.48352706263377));
#10644=CARTESIAN_POINT('Ctrl Pts',(3.35708792761402,-0.160839719007584,
1.44288889507334));
#10645=CARTESIAN_POINT('Ctrl Pts',(3.35789496093577,-0.165,1.42076875940744));
#10646=CARTESIAN_POINT('Ctrl Pts',(3.35789496093577,-0.165,1.37923124059256));
#10647=CARTESIAN_POINT('Ctrl Pts',(3.35708792761402,-0.160839719007584,
1.35711110492666));
#10648=CARTESIAN_POINT('Ctrl Pts',(3.35419203896924,-0.143986470216691,
1.31647293736623));
#10649=CARTESIAN_POINT('Ctrl Pts',(3.35214708226765,-0.131295993814186,
1.29795075602263));
#10650=CARTESIAN_POINT('Ctrl Pts',(3.34832345279534,-0.102049819008125,
1.26870458121656));
#10651=CARTESIAN_POINT('Ctrl Pts',(3.34629359821974,-0.0835273920906824,
1.25601365401642));
#10652=CARTESIAN_POINT('Ctrl Pts',(3.3434324152587,-0.0428883760934128,
1.23916007816136));
#10653=CARTESIAN_POINT('Ctrl Pts',(3.34264068711929,-0.0207679427235068,
1.235));
#10654=CARTESIAN_POINT('Ctrl Pts',(3.34264068711929,-4.16333634234434E-17,
1.235));
#10655=CARTESIAN_POINT('',(3.73764068711929,-1.70422299968729E-17,1.565));
#10656=CARTESIAN_POINT('',(3.24264069,-2.02066721859313E-17,1.565));
#10657=CARTESIAN_POINT('',(3.75264069,-0.122167928782887,1.51090535233657));
#10658=CARTESIAN_POINT('Ctrl Pts',(3.75264069,-0.122167928782887,1.51090535233657));
#10659=CARTESIAN_POINT('Ctrl Pts',(3.75219215735201,-0.120368921478644,
1.51288705106972));
#10660=CARTESIAN_POINT('Ctrl Pts',(3.75174544269427,-0.118534900551874,
1.51481033723969));
#10661=CARTESIAN_POINT('Ctrl Pts',(3.74784567158764,-0.102111993019358,
1.5312332447722));
#10662=CARTESIAN_POINT('Ctrl Pts',(3.74419817251169,-0.0836597150224319,
1.54390845611142));
#10663=CARTESIAN_POINT('Ctrl Pts',(3.73906286735823,-0.0430495960471595,
1.56079590960766));
#10664=CARTESIAN_POINT('Ctrl Pts',(3.73764068711929,-0.020880094330741,
1.565));
#10665=CARTESIAN_POINT('Ctrl Pts',(3.73764068711929,-2.08166817117217E-17,
1.565));
#10666=CARTESIAN_POINT('',(3.75264069,-0.122167928782887,1.28909464766343));
#10667=CARTESIAN_POINT('Origin',(3.75264069,0.,1.4));
#10668=CARTESIAN_POINT('',(3.73764068711929,-3.09223316784707E-17,1.235));
#10669=CARTESIAN_POINT('Ctrl Pts',(3.73764068711929,-1.38777878078145E-17,
1.235));
#10670=CARTESIAN_POINT('Ctrl Pts',(3.73764068711929,-0.020880094330741,
1.235));
#10671=CARTESIAN_POINT('Ctrl Pts',(3.73906286735823,-0.0430495960471595,
1.23920409039234));
#10672=CARTESIAN_POINT('Ctrl Pts',(3.74419817251169,-0.0836597150224319,
1.25609154388858));
#10673=CARTESIAN_POINT('Ctrl Pts',(3.74784567158764,-0.102111993019358,
1.2687667552278));
#10674=CARTESIAN_POINT('Ctrl Pts',(3.75174544269427,-0.118534900551874,
1.28518966276031));
#10675=CARTESIAN_POINT('Ctrl Pts',(3.75219215735201,-0.120368921478644,
1.28711294893028));
#10676=CARTESIAN_POINT('Ctrl Pts',(3.75264069,-0.122167928782887,1.28909464766343));
#10677=CARTESIAN_POINT('Ctrl Pts',(3.75264069,0.122167928782887,1.28909464766343));
#10678=CARTESIAN_POINT('Ctrl Pts',(3.75219215735201,0.120368921478644,1.28711294893028));
#10679=CARTESIAN_POINT('Ctrl Pts',(3.75174544269427,0.118534900551874,1.28518966276031));
#10680=CARTESIAN_POINT('Ctrl Pts',(3.74784567158764,0.102111993019358,1.2687667552278));
#10681=CARTESIAN_POINT('Ctrl Pts',(3.74419817251169,0.0836597150224319,
1.25609154388858));
#10682=CARTESIAN_POINT('Ctrl Pts',(3.73906286735823,0.0430495960471595,
1.23920409039234));
#10683=CARTESIAN_POINT('Ctrl Pts',(3.73764068711929,0.020880094330741,1.235));
#10684=CARTESIAN_POINT('Ctrl Pts',(3.73764068711929,0.,1.235));
#10685=CARTESIAN_POINT('Ctrl Pts',(3.73764068711929,-6.93889390390723E-18,
1.565));
#10686=CARTESIAN_POINT('Ctrl Pts',(3.73764068711929,0.020880094330741,1.565));
#10687=CARTESIAN_POINT('Ctrl Pts',(3.73906286735823,0.0430495960471595,
1.56079590960766));
#10688=CARTESIAN_POINT('Ctrl Pts',(3.74419817251169,0.0836597150224318,
1.54390845611142));
#10689=CARTESIAN_POINT('Ctrl Pts',(3.74784567158764,0.102111993019358,1.5312332447722));
#10690=CARTESIAN_POINT('Ctrl Pts',(3.75174544269427,0.118534900551874,1.51481033723969));
#10691=CARTESIAN_POINT('Ctrl Pts',(3.75219215735201,0.120368921478644,1.51288705106972));
#10692=CARTESIAN_POINT('Ctrl Pts',(3.75264069,0.122167928782887,1.51090535233657));
#10693=CARTESIAN_POINT('Origin',(3.75264069,0.,1.4));
#10694=CARTESIAN_POINT('',(3.75264069,-0.122167928782887,1.));
#10695=CARTESIAN_POINT('Origin',(4.24264068711929,0.,1.));
#10696=CARTESIAN_POINT('',(3.73764068711929,-6.18446633569413E-17,1.8));
#10697=CARTESIAN_POINT('Origin',(4.24264068711929,0.,1.8));
#10698=CARTESIAN_POINT('',(3.73764068711929,-6.18446633569413E-17,1.));
#10699=CARTESIAN_POINT('',(3.73764068711929,-6.18446633569413E-17,1.));
#10700=CARTESIAN_POINT('',(3.73764068711929,-6.18446633569413E-17,1.));
#10701=CARTESIAN_POINT('Origin',(4.24264068711929,0.,1.));
#10702=CARTESIAN_POINT('Origin',(4.24264068711929,0.,1.));
#10703=CARTESIAN_POINT('',(3.34264068711929,-1.10218211923262E-16,1.8));
#10704=CARTESIAN_POINT('Origin',(4.24264068711929,0.,1.8));
#10705=CARTESIAN_POINT('',(3.34264068711929,-1.10218211923262E-16,1.));
#10706=CARTESIAN_POINT('',(3.34264068711929,-1.10218211923262E-16,1.));
#10707=CARTESIAN_POINT('',(3.34264068711929,-1.10218211923262E-16,1.));
#10708=CARTESIAN_POINT('Origin',(4.24264068711929,0.,1.));
#10709=CARTESIAN_POINT('Origin',(4.24264068711929,0.,1.8));
#10710=CARTESIAN_POINT('Origin',(4.24264068711929,0.,1.));
#10805=UNCERTAINTY_MEASURE_WITH_UNIT(LENGTH_MEASURE(0.001),#10838,
'DISTANCE_ACCURACY_VALUE',
'Maximum model space distance between geometric entities at asserted c
onnectivities');
#10807=UNCERTAINTY_MEASURE_WITH_UNIT(LENGTH_MEASURE(0.001),#10838,
'DISTANCE_ACCURACY_VALUE',
'Maximum model space distance between geometric entities at asserted c
onnectivities');
#10835=(
GEOMETRIC_REPRESENTATION_CONTEXT(3)
GLOBAL_UNCERTAINTY_ASSIGNED_CONTEXT((#10805))
GLOBAL_UNIT_ASSIGNED_CONTEXT((#10838,#10840,#10841))
REPRESENTATION_CONTEXT('','3D')
);
#10837=(
GEOMETRIC_REPRESENTATION_CONTEXT(3)
GLOBAL_UNCERTAINTY_ASSIGNED_CONTEXT((#10807))
GLOBAL_UNIT_ASSIGNED_CONTEXT((#10838,#10840,#10841))
REPRESENTATION_CONTEXT('','3D')
);
#10838=(
LENGTH_UNIT()
NAMED_UNIT(*)
SI_UNIT(.CENTI.,.METRE.)
);
#10840=(
NAMED_UNIT(*)
PLANE_ANGLE_UNIT()
SI_UNIT($,.RADIAN.)
);
#10841=(
NAMED_UNIT(*)
SI_UNIT($,.STERADIAN.)
SOLID_ANGLE_UNIT()
);
#10869=SHAPE_DEFINITION_REPRESENTATION(#10922,#10968);
#10922=PRODUCT_DEFINITION_SHAPE('',$,#10998);
#10968=SHAPE_REPRESENTATION('',(#6614),#10835);
#10970=PRODUCT_DEFINITION_CONTEXT('part definition',#11059,'design');
#10998=PRODUCT_DEFINITION('Retaining collar (1)','Retaining collar (1)',#11027,
#10970);
#11027=PRODUCT_DEFINITION_FORMATION('',$,#11088);
#11059=APPLICATION_CONTEXT(
'Core Data for Automotive Mechanical Design Process');
#11060=PRODUCT_CONTEXT('part definition',#11059,'mechanical');
#11088=PRODUCT('Retaining collar (1)','Retaining collar (1)',
'Retaining collar (1)',(#11060));
#11174=COLOUR_RGB('Off White',0.89,0.88,0.83);
#11175=FILL_AREA_STYLE_COLOUR('',#11174);
#11176=FILL_AREA_STYLE('',(#11175));
#11177=SURFACE_STYLE_FILL_AREA(#11176);
#11178=SURFACE_SIDE_STYLE('',(#11177));
#11179=SURFACE_STYLE_USAGE(.BOTH.,#11178);
#11180=PRESENTATION_STYLE_ASSIGNMENT((#11179));
ENDSEC;
END-ISO-10303-21;
